ISO-10303-21;
HEADER;
/* Generated by software containing ST-Developer
 * from STEP Tools, Inc. (www.steptools.com) 
 */

FILE_DESCRIPTION(
/* description */ ('PAT-041'),
/* implementation_level */ '2;1');

FILE_NAME(
/* name */ 'Flange gasket (1).step',
/* time_stamp */ '2026-10-28T22:21:24-07:00',
/* author */ (''),
/* organization */ (''),
/* preprocessor_version */ 'ST-DEVELOPER v20.2',
/* originating_system */ 'Autodesk Translation Framework v15.17.0.0',
/* authorisation */ '');

FILE_SCHEMA (('AUTOMOTIVE_DESIGN { 1 0 10303 214 3 1 1 }'));
ENDSEC;

DATA;
#10=MECHANICAL_DESIGN_GEOMETRIC_PRESENTATION_REPRESENTATION('',(#215),#2507);
#195=SHAPE_REPRESENTATION_RELATIONSHIP('SRR','None',#2580,#205);
#205=ADVANCED_BREP_SHAPE_REPRESENTATION('',(#225),#2503);
#215=STYLED_ITEM('',(#2708),#225);
#225=MANIFOLD_SOLID_BREP('Body1',#1335);
#273=FACE_BOUND('',#471,.T.);
#274=FACE_BOUND('',#473,.T.);
#292=PLANE('',#1560);
#293=PLANE('',#1561);
#353=FACE_OUTER_BOUND('',#468,.T.);
#354=FACE_OUTER_BOUND('',#469,.T.);
#355=FACE_OUTER_BOUND('',#470,.T.);
#356=FACE_OUTER_BOUND('',#472,.T.);
#468=EDGE_LOOP('',(#1100,#1101,#1102,#1103));
#469=EDGE_LOOP('',(#1104,#1105,#1106,#1107));
#470=EDGE_LOOP('',(#1108));
#471=EDGE_LOOP('',(#1109));
#472=EDGE_LOOP('',(#1110));
#473=EDGE_LOOP('',(#1111));
#534=LINE('',#2277,#590);
#535=LINE('',#2283,#591);
#590=VECTOR('',#1883,1.065);
#591=VECTOR('',#1890,2.2);
#674=CIRCLE('',#1555,1.065);
#675=CIRCLE('',#1556,1.065);
#676=CIRCLE('',#1558,2.2);
#677=CIRCLE('',#1559,2.2);
#746=VERTEX_POINT('',#2274);
#747=VERTEX_POINT('',#2276);
#748=VERTEX_POINT('',#2280);
#749=VERTEX_POINT('',#2282);
#870=EDGE_CURVE('',#746,#746,#674,.T.);
#871=EDGE_CURVE('',#746,#747,#534,.T.);
#872=EDGE_CURVE('',#747,#747,#675,.T.);
#873=EDGE_CURVE('',#748,#748,#676,.T.);
#874=EDGE_CURVE('',#748,#749,#535,.T.);
#875=EDGE_CURVE('',#749,#749,#677,.T.);
#1100=ORIENTED_EDGE('',*,*,#870,.F.);
#1101=ORIENTED_EDGE('',*,*,#871,.T.);
#1102=ORIENTED_EDGE('',*,*,#872,.T.);
#1103=ORIENTED_EDGE('',*,*,#871,.F.);
#1104=ORIENTED_EDGE('',*,*,#873,.F.);
#1105=ORIENTED_EDGE('',*,*,#874,.T.);
#1106=ORIENTED_EDGE('',*,*,#875,.T.);
#1107=ORIENTED_EDGE('',*,*,#874,.F.);
#1108=ORIENTED_EDGE('',*,*,#873,.T.);
#1109=ORIENTED_EDGE('',*,*,#870,.T.);
#1110=ORIENTED_EDGE('',*,*,#875,.F.);
#1111=ORIENTED_EDGE('',*,*,#872,.F.);
#1252=CYLINDRICAL_SURFACE('',#1554,1.065);
#1253=CYLINDRICAL_SURFACE('',#1557,2.2);
#1298=ADVANCED_FACE('',(#353),#1252,.F.);
#1299=ADVANCED_FACE('',(#354),#1253,.T.);
#1300=ADVANCED_FACE('',(#355,#273),#292,.T.);
#1301=ADVANCED_FACE('',(#356,#274),#293,.F.);
#1335=CLOSED_SHELL('',(#1298,#1299,#1300,#1301));
#1553=AXIS2_PLACEMENT_3D('',#2272,#1877,#1878);
#1554=AXIS2_PLACEMENT_3D('',#2273,#1879,#1880);
#1555=AXIS2_PLACEMENT_3D('',#2275,#1881,#1882);
#1556=AXIS2_PLACEMENT_3D('',#2278,#1884,#1885);
#1557=AXIS2_PLACEMENT_3D('',#2279,#1886,#1887);
#1558=AXIS2_PLACEMENT_3D('',#2281,#1888,#1889);
#1559=AXIS2_PLACEMENT_3D('',#2284,#1891,#1892);
#1560=AXIS2_PLACEMENT_3D('',#2285,#1893,#1894);
#1561=AXIS2_PLACEMENT_3D('',#2286,#1895,#1896);
#1877=DIRECTION('axis',(0.,0.,1.));
#1878=DIRECTION('refdir',(1.,0.,0.));
#1879=DIRECTION('center_axis',(1.,0.,0.));
#1880=DIRECTION('ref_axis',(0.,0.,-1.));
#1881=DIRECTION('center_axis',(-1.,0.,0.));
#1882=DIRECTION('ref_axis',(0.,0.,-1.));
#1883=DIRECTION('',(-1.,0.,0.));
#1884=DIRECTION('center_axis',(-1.,0.,0.));
#1885=DIRECTION('ref_axis',(0.,0.,-1.));
#1886=DIRECTION('center_axis',(1.,0.,0.));
#1887=DIRECTION('ref_axis',(0.,0.,-1.));
#1888=DIRECTION('center_axis',(1.,0.,0.));
#1889=DIRECTION('ref_axis',(0.,0.,-1.));
#1890=DIRECTION('',(-1.,0.,0.));
#1891=DIRECTION('center_axis',(1.,0.,0.));
#1892=DIRECTION('ref_axis',(0.,0.,-1.));
#1893=DIRECTION('center_axis',(1.,0.,0.));
#1894=DIRECTION('ref_axis',(0.,0.,-1.));
#1895=DIRECTION('center_axis',(1.,0.,0.));
#1896=DIRECTION('ref_axis',(0.,0.,-1.));
#2272=CARTESIAN_POINT('',(0.,0.,0.));
#2273=CARTESIAN_POINT('Origin',(10.,0.,0.));
#2274=CARTESIAN_POINT('',(10.2,-1.30424884109193E-16,1.065));
#2275=CARTESIAN_POINT('Origin',(10.2,0.,0.));
#2276=CARTESIAN_POINT('',(10.,-1.30424884109193E-16,1.065));
#2277=CARTESIAN_POINT('',(10.,-1.30424884109193E-16,1.065));
#2278=CARTESIAN_POINT('Origin',(10.,0.,0.));
#2279=CARTESIAN_POINT('Origin',(10.,0.,0.));
#2280=CARTESIAN_POINT('',(10.2,-2.69422295812418E-16,2.2));
#2281=CARTESIAN_POINT('Origin',(10.2,0.,0.));
#2282=CARTESIAN_POINT('',(10.,-2.69422295812418E-16,2.2));
#2283=CARTESIAN_POINT('',(10.,-2.69422295812418E-16,2.2));
#2284=CARTESIAN_POINT('Origin',(10.,0.,0.));
#2285=CARTESIAN_POINT('Origin',(10.2,0.,0.));
#2286=CARTESIAN_POINT('Origin',(10.,0.,0.));
#2491=UNCERTAINTY_MEASURE_WITH_UNIT(LENGTH_MEASURE(0.001),#2508,
'DISTANCE_ACCURACY_VALUE',
'Maximum model space distance between geometric entities at asserted c
onnectivities');
#2495=UNCERTAINTY_MEASURE_WITH_UNIT(LENGTH_MEASURE(0.001),#2508,
'DISTANCE_ACCURACY_VALUE',
'Maximum model space distance between geometric entities at asserted c
onnectivities');
#2503=(
GEOMETRIC_REPRESENTATION_CONTEXT(3)
GLOBAL_UNCERTAINTY_ASSIGNED_CONTEXT((#2491))
GLOBAL_UNIT_ASSIGNED_CONTEXT((#2508,#2510,#2511))
REPRESENTATION_CONTEXT('','3D')
);
#2507=(
GEOMETRIC_REPRESENTATION_CONTEXT(3)
GLOBAL_UNCERTAINTY_ASSIGNED_CONTEXT((#2495))
GLOBAL_UNIT_ASSIGNED_CONTEXT((#2508,#2510,#2511))
REPRESENTATION_CONTEXT('','3D')
);
#2508=(
LENGTH_UNIT()
NAMED_UNIT(*)
SI_UNIT(.CENTI.,.METRE.)
);
#2510=(
NAMED_UNIT(*)
PLANE_ANGLE_UNIT()
SI_UNIT($,.RADIAN.)
);
#2511=(
NAMED_UNIT(*)
SI_UNIT($,.STERADIAN.)
SOLID_ANGLE_UNIT()
);
#2519=SHAPE_DEFINITION_REPRESENTATION(#2530,#2580);
#2530=PRODUCT_DEFINITION_SHAPE('',$,#2592);
#2580=SHAPE_REPRESENTATION('',(#1553),#2503);
#2584=PRODUCT_DEFINITION_CONTEXT('part definition',#2619,'design');
#2592=PRODUCT_DEFINITION('Flange gasket (1)',
'Flange gasket (1)',#2603,#2584);
#2603=PRODUCT_DEFINITION_FORMATION('',$,#2628);
#2619=APPLICATION_CONTEXT(
'Core Data for Automotive Mechanical Design Process');
#2620=PRODUCT_CONTEXT('part definition',#2619,'mechanical');
#2628=PRODUCT('Flange gasket (1)','Flange gasket (1)',
'Flange gasket (1)',(#2620));
#2702=COLOUR_RGB('Off White',0.89,0.88,0.83);
#2703=FILL_AREA_STYLE_COLOUR('',#2702);
#2704=FILL_AREA_STYLE('',(#2703));
#2705=SURFACE_STYLE_FILL_AREA(#2704);
#2706=SURFACE_SIDE_STYLE('',(#2705));
#2707=SURFACE_STYLE_USAGE(.BOTH.,#2706);
#2708=PRESENTATION_STYLE_ASSIGNMENT((#2707));
ENDSEC;
END-ISO-10303-21;
